ISO-10303-21;
HEADER;
/* Generated by software containing ST-Developer
 * from STEP Tools, Inc. (www.steptools.com) 
 */

FILE_DESCRIPTION(
/* description */ (''),
/* implementation_level */ '2;1');

FILE_NAME(
/* name */ '04_Shim_Washer_6.1x8x0.5.step',
/* time_stamp */ '2026-10-25T01:35:35-07:00',
/* author */ (''),
/* organization */ (''),
/* preprocessor_version */ 'ST-DEVELOPER v20.2',
/* originating_system */ 'Autodesk Translation Framework v15.15.0.0',
/* authorisation */ '');

FILE_SCHEMA (('AUTOMOTIVE_DESIGN { 1 0 10303 214 3 1 1 }'));
ENDSEC;

DATA;
#10=MECHANICAL_DESIGN_GEOMETRIC_PRESENTATION_REPRESENTATION('',(#263),#11430);
#239=SHAPE_REPRESENTATION_RELATIONSHIP('SRR','None',#11482,#251);
#251=ADVANCED_BREP_SHAPE_REPRESENTATION('',(#275),#11421);
#263=STYLED_ITEM('',(#11616),#275);
#275=MANIFOLD_SOLID_BREP('Body1',#4464);
#298=FACE_BOUND('',#876,.T.);
#299=FACE_BOUND('',#879,.T.);
#351=PLANE('',#4737);
#352=PLANE('',#4741);
#445=CYLINDRICAL_SURFACE('',#4734,3.05);
#446=CYLINDRICAL_SURFACE('',#4739,4.);
#592=FACE_OUTER_BOUND('',#874,.T.);
#593=FACE_OUTER_BOUND('',#875,.T.);
#594=FACE_OUTER_BOUND('',#877,.T.);
#595=FACE_OUTER_BOUND('',#878,.T.);
#874=EDGE_LOOP('',(#3135,#3136,#3137,#3138));
#875=EDGE_LOOP('',(#3139));
#876=EDGE_LOOP('',(#3140));
#877=EDGE_LOOP('',(#3141,#3142,#3143,#3144));
#878=EDGE_LOOP('',(#3145));
#879=EDGE_LOOP('',(#3146));
#1169=LINE('',#6600,#1459);
#1170=LINE('',#6608,#1460);
#1459=VECTOR('',#5411,3.05);
#1460=VECTOR('',#5422,4.);
#1738=CIRCLE('',#4735,3.05);
#1739=CIRCLE('',#4736,3.05);
#1740=CIRCLE('',#4738,4.);
#1741=CIRCLE('',#4740,4.);
#1939=VERTEX_POINT('',#6597);
#1940=VERTEX_POINT('',#6599);
#1941=VERTEX_POINT('',#6603);
#1942=VERTEX_POINT('',#6606);
#2385=EDGE_CURVE('',#1939,#1939,#1738,.T.);
#2386=EDGE_CURVE('',#1939,#1940,#1169,.T.);
#2387=EDGE_CURVE('',#1940,#1940,#1739,.T.);
#2388=EDGE_CURVE('',#1941,#1941,#1740,.T.);
#2389=EDGE_CURVE('',#1942,#1942,#1741,.T.);
#2390=EDGE_CURVE('',#1942,#1941,#1170,.T.);
#3135=ORIENTED_EDGE('',*,*,#2385,.T.);
#3136=ORIENTED_EDGE('',*,*,#2386,.T.);
#3137=ORIENTED_EDGE('',*,*,#2387,.F.);
#3138=ORIENTED_EDGE('',*,*,#2386,.F.);
#3139=ORIENTED_EDGE('',*,*,#2388,.F.);
#3140=ORIENTED_EDGE('',*,*,#2387,.T.);
#3141=ORIENTED_EDGE('',*,*,#2389,.F.);
#3142=ORIENTED_EDGE('',*,*,#2390,.T.);
#3143=ORIENTED_EDGE('',*,*,#2388,.T.);
#3144=ORIENTED_EDGE('',*,*,#2390,.F.);
#3145=ORIENTED_EDGE('',*,*,#2389,.T.);
#3146=ORIENTED_EDGE('',*,*,#2385,.F.);
#4259=ADVANCED_FACE('',(#592),#445,.F.);
#4260=ADVANCED_FACE('',(#593,#298),#351,.T.);
#4261=ADVANCED_FACE('',(#594),#446,.T.);
#4262=ADVANCED_FACE('',(#595,#299),#352,.T.);
#4464=CLOSED_SHELL('',(#4259,#4260,#4261,#4262));
#4733=AXIS2_PLACEMENT_3D('',#6595,#5405,#5406);
#4734=AXIS2_PLACEMENT_3D('',#6596,#5407,#5408);
#4735=AXIS2_PLACEMENT_3D('',#6598,#5409,#5410);
#4736=AXIS2_PLACEMENT_3D('',#6601,#5412,#5413);
#4737=AXIS2_PLACEMENT_3D('',#6602,#5414,#5415);
#4738=AXIS2_PLACEMENT_3D('',#6604,#5416,#5417);
#4739=AXIS2_PLACEMENT_3D('',#6605,#5418,#5419);
#4740=AXIS2_PLACEMENT_3D('',#6607,#5420,#5421);
#4741=AXIS2_PLACEMENT_3D('',#6609,#5423,#5424);
#5405=DIRECTION('axis',(0.,0.,1.));
#5406=DIRECTION('refdir',(1.,0.,0.));
#5407=DIRECTION('center_axis',(1.,0.,0.));
#5408=DIRECTION('ref_axis',(0.,1.,0.));
#5409=DIRECTION('center_axis',(1.,0.,0.));
#5410=DIRECTION('ref_axis',(0.,0.,-1.));
#5411=DIRECTION('',(-1.,0.,0.));
#5412=DIRECTION('center_axis',(1.,0.,0.));
#5413=DIRECTION('ref_axis',(0.,0.,-1.));
#5414=DIRECTION('center_axis',(-1.,0.,0.));
#5415=DIRECTION('ref_axis',(0.,0.,1.));
#5416=DIRECTION('center_axis',(1.,0.,0.));
#5417=DIRECTION('ref_axis',(0.,0.,-1.));
#5418=DIRECTION('center_axis',(1.,0.,0.));
#5419=DIRECTION('ref_axis',(0.,1.,0.));
#5420=DIRECTION('center_axis',(1.,0.,0.));
#5421=DIRECTION('ref_axis',(0.,0.,-1.));
#5422=DIRECTION('',(-1.,0.,0.));
#5423=DIRECTION('center_axis',(1.,0.,0.));
#5424=DIRECTION('ref_axis',(0.,0.,-1.));
#6595=CARTESIAN_POINT('',(0.,0.,0.));
#6596=CARTESIAN_POINT('Origin',(0.25,0.,0.));
#6597=CARTESIAN_POINT('',(0.5,-3.05,-3.73517273739943E-16));
#6598=CARTESIAN_POINT('Origin',(0.5,0.,0.));
#6599=CARTESIAN_POINT('',(0.,-3.05,-3.73517273739943E-16));
#6600=CARTESIAN_POINT('',(0.25,-3.05,-3.73517273739943E-16));
#6601=CARTESIAN_POINT('Origin',(0.,0.,0.));
#6602=CARTESIAN_POINT('Origin',(0.,4.,0.));
#6603=CARTESIAN_POINT('',(0.,-4.,-4.89858719658941E-16));
#6604=CARTESIAN_POINT('Origin',(0.,0.,0.));
#6605=CARTESIAN_POINT('Origin',(0.25,0.,0.));
#6606=CARTESIAN_POINT('',(0.5,-4.,-4.89858719658941E-16));
#6607=CARTESIAN_POINT('Origin',(0.5,0.,0.));
#6608=CARTESIAN_POINT('',(0.25,-4.,-4.89858719658941E-16));
#6609=CARTESIAN_POINT('Origin',(0.5,3.05,0.));
#11407=UNCERTAINTY_MEASURE_WITH_UNIT(LENGTH_MEASURE(0.01),#11431,
'DISTANCE_ACCURACY_VALUE',
'Maximum model space distance between geometric entities at asserted c
onnectivities');
#11416=UNCERTAINTY_MEASURE_WITH_UNIT(LENGTH_MEASURE(0.01),#11431,
'DISTANCE_ACCURACY_VALUE',
'Maximum model space distance between geometric entities at asserted c
onnectivities');
#11421=(
GEOMETRIC_REPRESENTATION_CONTEXT(3)
GLOBAL_UNCERTAINTY_ASSIGNED_CONTEXT((#11407))
GLOBAL_UNIT_ASSIGNED_CONTEXT((#11431,#11433,#11434))
REPRESENTATION_CONTEXT('','3D')
);
#11430=(
GEOMETRIC_REPRESENTATION_CONTEXT(3)
GLOBAL_UNCERTAINTY_ASSIGNED_CONTEXT((#11416))
GLOBAL_UNIT_ASSIGNED_CONTEXT((#11431,#11433,#11434))
REPRESENTATION_CONTEXT('','3D')
);
#11431=(
LENGTH_UNIT()
NAMED_UNIT(*)
SI_UNIT(.MILLI.,.METRE.)
);
#11433=(
NAMED_UNIT(*)
PLANE_ANGLE_UNIT()
SI_UNIT($,.RADIAN.)
);
#11434=(
NAMED_UNIT(*)
SI_UNIT($,.STERADIAN.)
SOLID_ANGLE_UNIT()
);
#11439=SHAPE_DEFINITION_REPRESENTATION(#11452,#11482);
#11452=PRODUCT_DEFINITION_SHAPE('',$,#11496);
#11482=SHAPE_REPRESENTATION('',(#4733),#11421);
#11491=PRODUCT_DEFINITION_CONTEXT('part definition',#11532,'design');
#11496=PRODUCT_DEFINITION('2026-10-25-00-55-37-835',
'04_Shim_Washer_6.1x8x0.5',#11509,#11491);
#11509=PRODUCT_DEFINITION_FORMATION('',$,#11538);
#11532=APPLICATION_CONTEXT(
'Core Data for Automotive Mechanical Design Process');
#11533=PRODUCT_CONTEXT('part definition',#11532,'mechanical');
#11538=PRODUCT('2026-10-25-00-55-37-835','04_Shim_Washer_6.1x8x0.5',$,(#11533));
#11610=COLOUR_RGB('Black',0.12,0.14,0.17);
#11611=FILL_AREA_STYLE_COLOUR('',#11610);
#11612=FILL_AREA_STYLE('',(#11611));
#11613=SURFACE_STYLE_FILL_AREA(#11612);
#11614=SURFACE_SIDE_STYLE('',(#11613));
#11615=SURFACE_STYLE_USAGE(.BOTH.,#11614);
#11616=PRESENTATION_STYLE_ASSIGNMENT((#11615));
ENDSEC;
END-ISO-10303-21;
